ISO-10303-21;
HEADER;
/* Generated by software containing ST-Developer
 * from STEP Tools, Inc. (www.steptools.com) 
 */

FILE_DESCRIPTION(
/* description */ ('Flywheel Crank-Slider'),
/* implementation_level */ '2;1');

FILE_NAME(
/* name */ 'Pin spacer 4 mm (1).step',
/* time_stamp */ '2026-10-28T03:23:13-07:00',
/* author */ (''),
/* organization */ (''),
/* preprocessor_version */ 'ST-DEVELOPER v20.2',
/* originating_system */ 'Autodesk Translation Framework v15.17.0.0',
/* authorisation */ '');

FILE_SCHEMA (('AUTOMOTIVE_DESIGN { 1 0 10303 214 3 1 1 }'));
ENDSEC;

DATA;
#10=MECHANICAL_DESIGN_GEOMETRIC_PRESENTATION_REPRESENTATION('',(#724),#17322);
#611=SHAPE_REPRESENTATION_RELATIONSHIP('SRR','None',#17612,#663);
#663=ADVANCED_BREP_SHAPE_REPRESENTATION('',(#781),#17316);
#724=STYLED_ITEM('',(#17931),#781);
#781=MANIFOLD_SOLID_BREP('Body1',#9106);
#995=FACE_BOUND('',#2554,.T.);
#996=FACE_BOUND('',#2556,.T.);
#1288=PLANE('',#10648);
#1289=PLANE('',#10649);
#1806=FACE_OUTER_BOUND('',#2551,.T.);
#1807=FACE_OUTER_BOUND('',#2552,.T.);
#1808=FACE_OUTER_BOUND('',#2553,.T.);
#1809=FACE_OUTER_BOUND('',#2555,.T.);
#2551=EDGE_LOOP('',(#8150,#8151,#8152,#8153));
#2552=EDGE_LOOP('',(#8154,#8155,#8156,#8157));
#2553=EDGE_LOOP('',(#8158));
#2554=EDGE_LOOP('',(#8159));
#2555=EDGE_LOOP('',(#8160));
#2556=EDGE_LOOP('',(#8161));
#3174=LINE('',#16905,#3785);
#3175=LINE('',#16911,#3786);
#3785=VECTOR('',#13306,0.505000000000001);
#3786=VECTOR('',#13313,0.699999999999999);
#4240=CIRCLE('',#10643,0.505000000000001);
#4241=CIRCLE('',#10644,0.505000000000001);
#4242=CIRCLE('',#10646,0.699999999999999);
#4243=CIRCLE('',#10647,0.699999999999999);
#4959=VERTEX_POINT('',#16902);
#4960=VERTEX_POINT('',#16904);
#4961=VERTEX_POINT('',#16908);
#4962=VERTEX_POINT('',#16910);
#6032=EDGE_CURVE('',#4959,#4959,#4240,.T.);
#6033=EDGE_CURVE('',#4959,#4960,#3174,.T.);
#6034=EDGE_CURVE('',#4960,#4960,#4241,.T.);
#6035=EDGE_CURVE('',#4961,#4961,#4242,.T.);
#6036=EDGE_CURVE('',#4961,#4962,#3175,.T.);
#6037=EDGE_CURVE('',#4962,#4962,#4243,.T.);
#8150=ORIENTED_EDGE('',*,*,#6032,.F.);
#8151=ORIENTED_EDGE('',*,*,#6033,.T.);
#8152=ORIENTED_EDGE('',*,*,#6034,.T.);
#8153=ORIENTED_EDGE('',*,*,#6033,.F.);
#8154=ORIENTED_EDGE('',*,*,#6035,.F.);
#8155=ORIENTED_EDGE('',*,*,#6036,.T.);
#8156=ORIENTED_EDGE('',*,*,#6037,.T.);
#8157=ORIENTED_EDGE('',*,*,#6036,.F.);
#8158=ORIENTED_EDGE('',*,*,#6035,.T.);
#8159=ORIENTED_EDGE('',*,*,#6032,.T.);
#8160=ORIENTED_EDGE('',*,*,#6037,.F.);
#8161=ORIENTED_EDGE('',*,*,#6034,.F.);
#8497=CYLINDRICAL_SURFACE('',#10642,0.505000000000001);
#8498=CYLINDRICAL_SURFACE('',#10645,0.699999999999999);
#8997=ADVANCED_FACE('',(#1806),#8497,.F.);
#8998=ADVANCED_FACE('',(#1807),#8498,.T.);
#8999=ADVANCED_FACE('',(#1808,#995),#1288,.T.);
#9000=ADVANCED_FACE('',(#1809,#996),#1289,.F.);
#9106=CLOSED_SHELL('',(#8997,#8998,#8999,#9000));
#10641=AXIS2_PLACEMENT_3D('',#16900,#13300,#13301);
#10642=AXIS2_PLACEMENT_3D('',#16901,#13302,#13303);
#10643=AXIS2_PLACEMENT_3D('',#16903,#13304,#13305);
#10644=AXIS2_PLACEMENT_3D('',#16906,#13307,#13308);
#10645=AXIS2_PLACEMENT_3D('',#16907,#13309,#13310);
#10646=AXIS2_PLACEMENT_3D('',#16909,#13311,#13312);
#10647=AXIS2_PLACEMENT_3D('',#16912,#13314,#13315);
#10648=AXIS2_PLACEMENT_3D('',#16913,#13316,#13317);
#10649=AXIS2_PLACEMENT_3D('',#16914,#13318,#13319);
#13300=DIRECTION('axis',(0.,0.,1.));
#13301=DIRECTION('refdir',(1.,0.,0.));
#13302=DIRECTION('center_axis',(0.,1.,0.));
#13303=DIRECTION('ref_axis',(1.,0.,0.));
#13304=DIRECTION('center_axis',(0.,-1.,0.));
#13305=DIRECTION('ref_axis',(1.,0.,0.));
#13306=DIRECTION('',(0.,-1.,0.));
#13307=DIRECTION('center_axis',(0.,-1.,0.));
#13308=DIRECTION('ref_axis',(1.,0.,0.));
#13309=DIRECTION('center_axis',(0.,1.,0.));
#13310=DIRECTION('ref_axis',(1.,0.,0.));
#13311=DIRECTION('center_axis',(0.,1.,0.));
#13312=DIRECTION('ref_axis',(1.,0.,0.));
#13313=DIRECTION('',(0.,-1.,0.));
#13314=DIRECTION('center_axis',(0.,1.,0.));
#13315=DIRECTION('ref_axis',(1.,0.,0.));
#13316=DIRECTION('center_axis',(0.,1.,0.));
#13317=DIRECTION('ref_axis',(1.,0.,0.));
#13318=DIRECTION('center_axis',(0.,1.,0.));
#13319=DIRECTION('ref_axis',(1.,0.,0.));
#16900=CARTESIAN_POINT('',(0.,0.,0.));
#16901=CARTESIAN_POINT('Origin',(12.,3.4,10.));
#16902=CARTESIAN_POINT('',(11.495,3.8,10.));
#16903=CARTESIAN_POINT('Origin',(12.,3.8,10.));
#16904=CARTESIAN_POINT('',(11.495,3.4,10.));
#16905=CARTESIAN_POINT('',(11.495,3.4,10.));
#16906=CARTESIAN_POINT('Origin',(12.,3.4,10.));
#16907=CARTESIAN_POINT('Origin',(12.,3.4,10.));
#16908=CARTESIAN_POINT('',(11.3,3.8,10.));
#16909=CARTESIAN_POINT('Origin',(12.,3.8,10.));
#16910=CARTESIAN_POINT('',(11.3,3.4,10.));
#16911=CARTESIAN_POINT('',(11.3,3.4,10.));
#16912=CARTESIAN_POINT('Origin',(12.,3.4,10.));
#16913=CARTESIAN_POINT('Origin',(12.,3.8,10.));
#16914=CARTESIAN_POINT('Origin',(12.,3.4,10.));
#17255=UNCERTAINTY_MEASURE_WITH_UNIT(LENGTH_MEASURE(0.001),#17323,
'DISTANCE_ACCURACY_VALUE',
'Maximum model space distance between geometric entities at asserted c
onnectivities');
#17261=UNCERTAINTY_MEASURE_WITH_UNIT(LENGTH_MEASURE(0.001),#17323,
'DISTANCE_ACCURACY_VALUE',
'Maximum model space distance between geometric entities at asserted c
onnectivities');
#17316=(
GEOMETRIC_REPRESENTATION_CONTEXT(3)
GLOBAL_UNCERTAINTY_ASSIGNED_CONTEXT((#17255))
GLOBAL_UNIT_ASSIGNED_CONTEXT((#17323,#17325,#17326))
REPRESENTATION_CONTEXT('','3D')
);
#17322=(
GEOMETRIC_REPRESENTATION_CONTEXT(3)
GLOBAL_UNCERTAINTY_ASSIGNED_CONTEXT((#17261))
GLOBAL_UNIT_ASSIGNED_CONTEXT((#17323,#17325,#17326))
REPRESENTATION_CONTEXT('','3D')
);
#17323=(
LENGTH_UNIT()
NAMED_UNIT(*)
SI_UNIT(.CENTI.,.METRE.)
);
#17325=(
NAMED_UNIT(*)
PLANE_ANGLE_UNIT()
SI_UNIT($,.RADIAN.)
);
#17326=(
NAMED_UNIT(*)
SI_UNIT($,.STERADIAN.)
SOLID_ANGLE_UNIT()
);
#17381=SHAPE_DEFINITION_REPRESENTATION(#17455,#17612);
#17455=PRODUCT_DEFINITION_SHAPE('',$,#17673);
#17612=SHAPE_REPRESENTATION('',(#10641),#17316);
#17618=PRODUCT_DEFINITION_CONTEXT('part definition',#17800,'design');
#17673=PRODUCT_DEFINITION('Pin spacer 4 mm (1)','Pin spacer 4 mm (1)',#17733,
#17618);
#17733=PRODUCT_DEFINITION_FORMATION('',$,#17856);
#17800=APPLICATION_CONTEXT(
'Core Data for Automotive Mechanical Design Process');
#17801=PRODUCT_CONTEXT('part definition',#17800,'mechanical');
#17856=PRODUCT('Pin spacer 4 mm (1)','Pin spacer 4 mm (1)',
'Pin spacer 4 mm (1)',(#17801));
#17925=COLOUR_RGB('Grey',0.48,0.52,0.57);
#17926=FILL_AREA_STYLE_COLOUR('',#17925);
#17927=FILL_AREA_STYLE('',(#17926));
#17928=SURFACE_STYLE_FILL_AREA(#17927);
#17929=SURFACE_SIDE_STYLE('',(#17928));
#17930=SURFACE_STYLE_USAGE(.BOTH.,#17929);
#17931=PRESENTATION_STYLE_ASSIGNMENT((#17930));
ENDSEC;
END-ISO-10303-21;
